ISO-10303-21;
HEADER;
/* Generated by software containing ST-Developer
 * from STEP Tools, Inc. (www.steptools.com) 
 */

FILE_DESCRIPTION(
/* description */ ('Rotary union on bearing shaft'),
/* implementation_level */ '2;1');

FILE_NAME(
/* name */ 'Bearing cap (1).step',
/* time_stamp */ '2026-10-28T03:24:01-07:00',
/* author */ (''),
/* organization */ (''),
/* preprocessor_version */ 'ST-DEVELOPER v20.2',
/* originating_system */ 'Autodesk Translation Framework v15.17.0.0',
/* authorisation */ '');

FILE_SCHEMA (('AUTOMOTIVE_DESIGN { 1 0 10303 214 3 1 1 }'));
ENDSEC;

DATA;
#10=MECHANICAL_DESIGN_GEOMETRIC_PRESENTATION_REPRESENTATION('',(#321),#9448);
#267=SHAPE_REPRESENTATION_RELATIONSHIP('SRR','None',#9567,#294);
#294=ADVANCED_BREP_SHAPE_REPRESENTATION('',(#356),#9427);
#321=STYLED_ITEM('',(#9778),#356);
#356=MANIFOLD_SOLID_BREP('Body1',#4876);
#433=FACE_BOUND('',#1103,.T.);
#434=FACE_BOUND('',#1107,.T.);
#435=FACE_BOUND('',#1108,.T.);
#436=FACE_BOUND('',#1109,.T.);
#437=FACE_BOUND('',#1110,.T.);
#438=FACE_BOUND('',#1111,.T.);
#439=FACE_BOUND('',#1113,.T.);
#440=FACE_BOUND('',#1114,.T.);
#441=FACE_BOUND('',#1115,.T.);
#442=FACE_BOUND('',#1116,.T.);
#443=FACE_BOUND('',#1117,.T.);
#535=PLANE('',#5404);
#536=PLANE('',#5411);
#537=PLANE('',#5412);
#745=FACE_OUTER_BOUND('',#1097,.T.);
#746=FACE_OUTER_BOUND('',#1098,.T.);
#747=FACE_OUTER_BOUND('',#1099,.T.);
#748=FACE_OUTER_BOUND('',#1100,.T.);
#749=FACE_OUTER_BOUND('',#1101,.T.);
#750=FACE_OUTER_BOUND('',#1102,.T.);
#751=FACE_OUTER_BOUND('',#1104,.T.);
#752=FACE_OUTER_BOUND('',#1105,.T.);
#753=FACE_OUTER_BOUND('',#1106,.T.);
#754=FACE_OUTER_BOUND('',#1112,.T.);
#1097=EDGE_LOOP('',(#3633,#3634,#3635,#3636));
#1098=EDGE_LOOP('',(#3637,#3638,#3639,#3640));
#1099=EDGE_LOOP('',(#3641,#3642,#3643,#3644));
#1100=EDGE_LOOP('',(#3645,#3646,#3647,#3648));
#1101=EDGE_LOOP('',(#3649,#3650,#3651,#3652));
#1102=EDGE_LOOP('',(#3653));
#1103=EDGE_LOOP('',(#3654));
#1104=EDGE_LOOP('',(#3655,#3656,#3657,#3658));
#1105=EDGE_LOOP('',(#3659,#3660,#3661,#3662));
#1106=EDGE_LOOP('',(#3663));
#1107=EDGE_LOOP('',(#3664));
#1108=EDGE_LOOP('',(#3665));
#1109=EDGE_LOOP('',(#3666));
#1110=EDGE_LOOP('',(#3667));
#1111=EDGE_LOOP('',(#3668));
#1112=EDGE_LOOP('',(#3669));
#1113=EDGE_LOOP('',(#3670));
#1114=EDGE_LOOP('',(#3671));
#1115=EDGE_LOOP('',(#3672));
#1116=EDGE_LOOP('',(#3673));
#1117=EDGE_LOOP('',(#3674));
#1451=LINE('',#7933,#1771);
#1452=LINE('',#7939,#1772);
#1453=LINE('',#7945,#1773);
#1454=LINE('',#7951,#1774);
#1455=LINE('',#7957,#1775);
#1456=LINE('',#7965,#1776);
#1457=LINE('',#7970,#1777);
#1771=VECTOR('',#6292,0.225);
#1772=VECTOR('',#6299,0.225);
#1773=VECTOR('',#6306,0.225);
#1774=VECTOR('',#6313,0.225);
#1775=VECTOR('',#6320,2.34);
#1776=VECTOR('',#6331,1.8);
#1777=VECTOR('',#6336,3.5);
#2086=CIRCLE('',#5390,0.225);
#2087=CIRCLE('',#5391,0.225);
#2088=CIRCLE('',#5393,0.225);
#2089=CIRCLE('',#5394,0.225);
#2090=CIRCLE('',#5396,0.225);
#2091=CIRCLE('',#5397,0.225);
#2092=CIRCLE('',#5399,0.225);
#2093=CIRCLE('',#5400,0.225);
#2094=CIRCLE('',#5402,2.34);
#2095=CIRCLE('',#5403,2.34);
#2096=CIRCLE('',#5405,1.8);
#2097=CIRCLE('',#5407,1.8);
#2098=CIRCLE('',#5409,3.5);
#2099=CIRCLE('',#5410,3.5);
#2374=VERTEX_POINT('',#7930);
#2375=VERTEX_POINT('',#7932);
#2376=VERTEX_POINT('',#7936);
#2377=VERTEX_POINT('',#7938);
#2378=VERTEX_POINT('',#7942);
#2379=VERTEX_POINT('',#7944);
#2380=VERTEX_POINT('',#7948);
#2381=VERTEX_POINT('',#7950);
#2382=VERTEX_POINT('',#7954);
#2383=VERTEX_POINT('',#7956);
#2384=VERTEX_POINT('',#7960);
#2385=VERTEX_POINT('',#7963);
#2386=VERTEX_POINT('',#7967);
#2387=VERTEX_POINT('',#7969);
#2844=EDGE_CURVE('',#2374,#2374,#2086,.T.);
#2845=EDGE_CURVE('',#2374,#2375,#1451,.T.);
#2846=EDGE_CURVE('',#2375,#2375,#2087,.T.);
#2847=EDGE_CURVE('',#2376,#2376,#2088,.T.);
#2848=EDGE_CURVE('',#2376,#2377,#1452,.T.);
#2849=EDGE_CURVE('',#2377,#2377,#2089,.T.);
#2850=EDGE_CURVE('',#2378,#2378,#2090,.T.);
#2851=EDGE_CURVE('',#2378,#2379,#1453,.T.);
#2852=EDGE_CURVE('',#2379,#2379,#2091,.T.);
#2853=EDGE_CURVE('',#2380,#2380,#2092,.T.);
#2854=EDGE_CURVE('',#2380,#2381,#1454,.T.);
#2855=EDGE_CURVE('',#2381,#2381,#2093,.T.);
#2856=EDGE_CURVE('',#2382,#2382,#2094,.T.);
#2857=EDGE_CURVE('',#2382,#2383,#1455,.T.);
#2858=EDGE_CURVE('',#2383,#2383,#2095,.T.);
#2859=EDGE_CURVE('',#2384,#2384,#2096,.T.);
#2860=EDGE_CURVE('',#2385,#2385,#2097,.T.);
#2861=EDGE_CURVE('',#2385,#2384,#1456,.T.);
#2862=EDGE_CURVE('',#2386,#2386,#2098,.T.);
#2863=EDGE_CURVE('',#2386,#2387,#1457,.T.);
#2864=EDGE_CURVE('',#2387,#2387,#2099,.T.);
#3633=ORIENTED_EDGE('',*,*,#2844,.F.);
#3634=ORIENTED_EDGE('',*,*,#2845,.T.);
#3635=ORIENTED_EDGE('',*,*,#2846,.F.);
#3636=ORIENTED_EDGE('',*,*,#2845,.F.);
#3637=ORIENTED_EDGE('',*,*,#2847,.F.);
#3638=ORIENTED_EDGE('',*,*,#2848,.T.);
#3639=ORIENTED_EDGE('',*,*,#2849,.F.);
#3640=ORIENTED_EDGE('',*,*,#2848,.F.);
#3641=ORIENTED_EDGE('',*,*,#2850,.F.);
#3642=ORIENTED_EDGE('',*,*,#2851,.T.);
#3643=ORIENTED_EDGE('',*,*,#2852,.F.);
#3644=ORIENTED_EDGE('',*,*,#2851,.F.);
#3645=ORIENTED_EDGE('',*,*,#2853,.F.);
#3646=ORIENTED_EDGE('',*,*,#2854,.T.);
#3647=ORIENTED_EDGE('',*,*,#2855,.F.);
#3648=ORIENTED_EDGE('',*,*,#2854,.F.);
#3649=ORIENTED_EDGE('',*,*,#2856,.F.);
#3650=ORIENTED_EDGE('',*,*,#2857,.T.);
#3651=ORIENTED_EDGE('',*,*,#2858,.T.);
#3652=ORIENTED_EDGE('',*,*,#2857,.F.);
#3653=ORIENTED_EDGE('',*,*,#2858,.F.);
#3654=ORIENTED_EDGE('',*,*,#2859,.F.);
#3655=ORIENTED_EDGE('',*,*,#2860,.F.);
#3656=ORIENTED_EDGE('',*,*,#2861,.T.);
#3657=ORIENTED_EDGE('',*,*,#2859,.T.);
#3658=ORIENTED_EDGE('',*,*,#2861,.F.);
#3659=ORIENTED_EDGE('',*,*,#2862,.F.);
#3660=ORIENTED_EDGE('',*,*,#2863,.T.);
#3661=ORIENTED_EDGE('',*,*,#2864,.T.);
#3662=ORIENTED_EDGE('',*,*,#2863,.F.);
#3663=ORIENTED_EDGE('',*,*,#2862,.T.);
#3664=ORIENTED_EDGE('',*,*,#2860,.T.);
#3665=ORIENTED_EDGE('',*,*,#2855,.T.);
#3666=ORIENTED_EDGE('',*,*,#2852,.T.);
#3667=ORIENTED_EDGE('',*,*,#2849,.T.);
#3668=ORIENTED_EDGE('',*,*,#2846,.T.);
#3669=ORIENTED_EDGE('',*,*,#2864,.F.);
#3670=ORIENTED_EDGE('',*,*,#2856,.T.);
#3671=ORIENTED_EDGE('',*,*,#2853,.T.);
#3672=ORIENTED_EDGE('',*,*,#2850,.T.);
#3673=ORIENTED_EDGE('',*,*,#2847,.T.);
#3674=ORIENTED_EDGE('',*,*,#2844,.T.);
#4518=CYLINDRICAL_SURFACE('',#5389,0.225);
#4519=CYLINDRICAL_SURFACE('',#5392,0.225);
#4520=CYLINDRICAL_SURFACE('',#5395,0.225);
#4521=CYLINDRICAL_SURFACE('',#5398,0.225);
#4522=CYLINDRICAL_SURFACE('',#5401,2.34);
#4523=CYLINDRICAL_SURFACE('',#5406,1.8);
#4524=CYLINDRICAL_SURFACE('',#5408,3.5);
#4658=ADVANCED_FACE('',(#745),#4518,.F.);
#4659=ADVANCED_FACE('',(#746),#4519,.F.);
#4660=ADVANCED_FACE('',(#747),#4520,.F.);
#4661=ADVANCED_FACE('',(#748),#4521,.F.);
#4662=ADVANCED_FACE('',(#749),#4522,.T.);
#4663=ADVANCED_FACE('',(#750,#433),#535,.F.);
#4664=ADVANCED_FACE('',(#751),#4523,.F.);
#4665=ADVANCED_FACE('',(#752),#4524,.T.);
#4666=ADVANCED_FACE('',(#753,#434,#435,#436,#437,#438),#536,.T.);
#4667=ADVANCED_FACE('',(#754,#439,#440,#441,#442,#443),#537,.F.);
#4876=CLOSED_SHELL('',(#4658,#4659,#4660,#4661,#4662,#4663,#4664,#4665,
#4666,#4667));
#5388=AXIS2_PLACEMENT_3D('',#7928,#6286,#6287);
#5389=AXIS2_PLACEMENT_3D('',#7929,#6288,#6289);
#5390=AXIS2_PLACEMENT_3D('',#7931,#6290,#6291);
#5391=AXIS2_PLACEMENT_3D('',#7934,#6293,#6294);
#5392=AXIS2_PLACEMENT_3D('',#7935,#6295,#6296);
#5393=AXIS2_PLACEMENT_3D('',#7937,#6297,#6298);
#5394=AXIS2_PLACEMENT_3D('',#7940,#6300,#6301);
#5395=AXIS2_PLACEMENT_3D('',#7941,#6302,#6303);
#5396=AXIS2_PLACEMENT_3D('',#7943,#6304,#6305);
#5397=AXIS2_PLACEMENT_3D('',#7946,#6307,#6308);
#5398=AXIS2_PLACEMENT_3D('',#7947,#6309,#6310);
#5399=AXIS2_PLACEMENT_3D('',#7949,#6311,#6312);
#5400=AXIS2_PLACEMENT_3D('',#7952,#6314,#6315);
#5401=AXIS2_PLACEMENT_3D('',#7953,#6316,#6317);
#5402=AXIS2_PLACEMENT_3D('',#7955,#6318,#6319);
#5403=AXIS2_PLACEMENT_3D('',#7958,#6321,#6322);
#5404=AXIS2_PLACEMENT_3D('',#7959,#6323,#6324);
#5405=AXIS2_PLACEMENT_3D('',#7961,#6325,#6326);
#5406=AXIS2_PLACEMENT_3D('',#7962,#6327,#6328);
#5407=AXIS2_PLACEMENT_3D('',#7964,#6329,#6330);
#5408=AXIS2_PLACEMENT_3D('',#7966,#6332,#6333);
#5409=AXIS2_PLACEMENT_3D('',#7968,#6334,#6335);
#5410=AXIS2_PLACEMENT_3D('',#7971,#6337,#6338);
#5411=AXIS2_PLACEMENT_3D('',#7972,#6339,#6340);
#5412=AXIS2_PLACEMENT_3D('',#7973,#6341,#6342);
#6286=DIRECTION('axis',(0.,0.,1.));
#6287=DIRECTION('refdir',(1.,0.,0.));
#6288=DIRECTION('center_axis',(0.,1.,0.));
#6289=DIRECTION('ref_axis',(1.,0.,0.));
#6290=DIRECTION('center_axis',(0.,1.,0.));
#6291=DIRECTION('ref_axis',(1.,0.,0.));
#6292=DIRECTION('',(0.,1.,0.));
#6293=DIRECTION('center_axis',(0.,-1.,0.));
#6294=DIRECTION('ref_axis',(1.,0.,0.));
#6295=DIRECTION('center_axis',(0.,1.,0.));
#6296=DIRECTION('ref_axis',(1.,0.,0.));
#6297=DIRECTION('center_axis',(0.,1.,0.));
#6298=DIRECTION('ref_axis',(1.,0.,0.));
#6299=DIRECTION('',(0.,1.,0.));
#6300=DIRECTION('center_axis',(0.,-1.,0.));
#6301=DIRECTION('ref_axis',(1.,0.,0.));
#6302=DIRECTION('center_axis',(0.,1.,0.));
#6303=DIRECTION('ref_axis',(1.,0.,0.));
#6304=DIRECTION('center_axis',(0.,1.,0.));
#6305=DIRECTION('ref_axis',(1.,0.,0.));
#6306=DIRECTION('',(0.,1.,0.));
#6307=DIRECTION('center_axis',(0.,-1.,0.));
#6308=DIRECTION('ref_axis',(1.,0.,0.));
#6309=DIRECTION('center_axis',(0.,1.,0.));
#6310=DIRECTION('ref_axis',(1.,0.,0.));
#6311=DIRECTION('center_axis',(0.,1.,0.));
#6312=DIRECTION('ref_axis',(1.,0.,0.));
#6313=DIRECTION('',(0.,1.,0.));
#6314=DIRECTION('center_axis',(0.,-1.,0.));
#6315=DIRECTION('ref_axis',(1.,0.,0.));
#6316=DIRECTION('center_axis',(0.,1.,0.));
#6317=DIRECTION('ref_axis',(1.,0.,0.));
#6318=DIRECTION('center_axis',(0.,1.,0.));
#6319=DIRECTION('ref_axis',(1.,0.,0.));
#6320=DIRECTION('',(0.,-1.,0.));
#6321=DIRECTION('center_axis',(0.,1.,0.));
#6322=DIRECTION('ref_axis',(1.,0.,0.));
#6323=DIRECTION('center_axis',(0.,1.,0.));
#6324=DIRECTION('ref_axis',(1.,0.,0.));
#6325=DIRECTION('center_axis',(0.,-1.,0.));
#6326=DIRECTION('ref_axis',(1.,0.,0.));
#6327=DIRECTION('center_axis',(0.,1.,0.));
#6328=DIRECTION('ref_axis',(1.,0.,0.));
#6329=DIRECTION('center_axis',(0.,-1.,0.));
#6330=DIRECTION('ref_axis',(1.,0.,0.));
#6331=DIRECTION('',(0.,-1.,0.));
#6332=DIRECTION('center_axis',(0.,1.,0.));
#6333=DIRECTION('ref_axis',(1.,0.,0.));
#6334=DIRECTION('center_axis',(0.,1.,0.));
#6335=DIRECTION('ref_axis',(1.,0.,0.));
#6336=DIRECTION('',(0.,-1.,0.));
#6337=DIRECTION('center_axis',(0.,1.,0.));
#6338=DIRECTION('ref_axis',(1.,0.,0.));
#6339=DIRECTION('center_axis',(0.,1.,0.));
#6340=DIRECTION('ref_axis',(1.,0.,0.));
#6341=DIRECTION('center_axis',(0.,1.,0.));
#6342=DIRECTION('ref_axis',(1.,0.,0.));
#7928=CARTESIAN_POINT('',(0.,0.,0.));
#7929=CARTESIAN_POINT('Origin',(-2.8,5.9,4.5));
#7930=CARTESIAN_POINT('',(-3.025,6.,4.5));
#7931=CARTESIAN_POINT('Origin',(-2.8,6.,4.5));
#7932=CARTESIAN_POINT('',(-3.025,6.4,4.5));
#7933=CARTESIAN_POINT('',(-3.025,5.9,4.5));
#7934=CARTESIAN_POINT('Origin',(-2.8,6.4,4.5));
#7935=CARTESIAN_POINT('Origin',(1.71450551880629E-16,5.9,7.3));
#7936=CARTESIAN_POINT('',(-0.225,6.,7.3));
#7937=CARTESIAN_POINT('Origin',(1.71450551880629E-16,6.,7.3));
#7938=CARTESIAN_POINT('',(-0.225,6.4,7.3));
#7939=CARTESIAN_POINT('',(-0.225,5.9,7.3));
#7940=CARTESIAN_POINT('Origin',(1.71450551880629E-16,6.4,7.3));
#7941=CARTESIAN_POINT('Origin',(2.8,5.9,4.5));
#7942=CARTESIAN_POINT('',(2.575,6.,4.5));
#7943=CARTESIAN_POINT('Origin',(2.8,6.,4.5));
#7944=CARTESIAN_POINT('',(2.575,6.4,4.5));
#7945=CARTESIAN_POINT('',(2.575,5.9,4.5));
#7946=CARTESIAN_POINT('Origin',(2.8,6.4,4.5));
#7947=CARTESIAN_POINT('Origin',(-5.14351655641888E-16,5.9,1.7));
#7948=CARTESIAN_POINT('',(-0.225000000000001,6.,1.7));
#7949=CARTESIAN_POINT('Origin',(-5.14351655641888E-16,6.,1.7));
#7950=CARTESIAN_POINT('',(-0.225000000000001,6.4,1.7));
#7951=CARTESIAN_POINT('',(-0.225000000000001,5.9,1.7));
#7952=CARTESIAN_POINT('Origin',(-5.14351655641888E-16,6.4,1.7));
#7953=CARTESIAN_POINT('Origin',(0.,5.7,4.5));
#7954=CARTESIAN_POINT('',(-2.34,6.,4.5));
#7955=CARTESIAN_POINT('Origin',(0.,6.,4.5));
#7956=CARTESIAN_POINT('',(-2.34,5.7,4.5));
#7957=CARTESIAN_POINT('',(-2.34,5.7,4.5));
#7958=CARTESIAN_POINT('Origin',(0.,5.7,4.5));
#7959=CARTESIAN_POINT('Origin',(0.,5.7,4.5));
#7960=CARTESIAN_POINT('',(-1.8,5.7,4.5));
#7961=CARTESIAN_POINT('Origin',(0.,5.7,4.5));
#7962=CARTESIAN_POINT('Origin',(0.,6.,4.5));
#7963=CARTESIAN_POINT('',(-1.8,6.4,4.5));
#7964=CARTESIAN_POINT('Origin',(0.,6.4,4.5));
#7965=CARTESIAN_POINT('',(-1.8,6.,4.5));
#7966=CARTESIAN_POINT('Origin',(0.,6.,4.5));
#7967=CARTESIAN_POINT('',(-3.5,6.4,4.5));
#7968=CARTESIAN_POINT('Origin',(0.,6.4,4.5));
#7969=CARTESIAN_POINT('',(-3.5,6.,4.5));
#7970=CARTESIAN_POINT('',(-3.5,6.,4.5));
#7971=CARTESIAN_POINT('Origin',(0.,6.,4.5));
#7972=CARTESIAN_POINT('Origin',(0.,6.4,4.5));
#7973=CARTESIAN_POINT('Origin',(0.,6.,4.5));
#9395=UNCERTAINTY_MEASURE_WITH_UNIT(LENGTH_MEASURE(0.001),#9449,
'DISTANCE_ACCURACY_VALUE',
'Maximum model space distance between geometric entities at asserted c
onnectivities');
#9416=UNCERTAINTY_MEASURE_WITH_UNIT(LENGTH_MEASURE(0.001),#9449,
'DISTANCE_ACCURACY_VALUE',
'Maximum model space distance between geometric entities at asserted c
onnectivities');
#9427=(
GEOMETRIC_REPRESENTATION_CONTEXT(3)
GLOBAL_UNCERTAINTY_ASSIGNED_CONTEXT((#9395))
GLOBAL_UNIT_ASSIGNED_CONTEXT((#9449,#9451,#9452))
REPRESENTATION_CONTEXT('','3D')
);
#9448=(
GEOMETRIC_REPRESENTATION_CONTEXT(3)
GLOBAL_UNCERTAINTY_ASSIGNED_CONTEXT((#9416))
GLOBAL_UNIT_ASSIGNED_CONTEXT((#9449,#9451,#9452))
REPRESENTATION_CONTEXT('','3D')
);
#9449=(
LENGTH_UNIT()
NAMED_UNIT(*)
SI_UNIT(.CENTI.,.METRE.)
);
#9451=(
NAMED_UNIT(*)
PLANE_ANGLE_UNIT()
SI_UNIT($,.RADIAN.)
);
#9452=(
NAMED_UNIT(*)
SI_UNIT($,.STERADIAN.)
SOLID_ANGLE_UNIT()
);
#9463=SHAPE_DEFINITION_REPRESENTATION(#9494,#9567);
#9494=PRODUCT_DEFINITION_SHAPE('',$,#9599);
#9567=SHAPE_REPRESENTATION('',(#5388),#9427);
#9588=PRODUCT_DEFINITION_CONTEXT('part definition',#9683,'design');
#9599=PRODUCT_DEFINITION('Bearing cap (1)','Bearing cap (1)',#9630,#9588);
#9630=PRODUCT_DEFINITION_FORMATION('',$,#9695);
#9683=APPLICATION_CONTEXT(
'Core Data for Automotive Mechanical Design Process');
#9684=PRODUCT_CONTEXT('part definition',#9683,'mechanical');
#9695=PRODUCT('Bearing cap (1)','Bearing cap (1)','Bearing cap (1)',(#9684));
#9772=COLOUR_RGB('Grey',0.48,0.52,0.57);
#9773=FILL_AREA_STYLE_COLOUR('',#9772);
#9774=FILL_AREA_STYLE('',(#9773));
#9775=SURFACE_STYLE_FILL_AREA(#9774);
#9776=SURFACE_SIDE_STYLE('',(#9775));
#9777=SURFACE_STYLE_USAGE(.BOTH.,#9776);
#9778=PRESENTATION_STYLE_ASSIGNMENT((#9777));
ENDSEC;
END-ISO-10303-21;
